ISO-10303-21;
HEADER;
/* Generated by software containing ST-Developer
 * from STEP Tools, Inc. (www.steptools.com) 
 */

FILE_DESCRIPTION(
/* description */ ('Counterbalanced vertical column'),
/* implementation_level */ '2;1');

FILE_NAME(
/* name */ 'M4 top nut.step',
/* time_stamp */ '2026-10-29T16:47:22-07:00',
/* author */ (''),
/* organization */ (''),
/* preprocessor_version */ 'ST-DEVELOPER v20.2',
/* originating_system */ 'Autodesk Translation Framework v15.17.0.0',
/* authorisation */ '');

FILE_SCHEMA (('AUTOMOTIVE_DESIGN { 1 0 10303 214 3 1 1 }'));
ENDSEC;

DATA;
#10=MECHANICAL_DESIGN_GEOMETRIC_PRESENTATION_REPRESENTATION('',(#361),#15040);
#291=SHAPE_REPRESENTATION_RELATIONSHIP('SRR','None',#15195,#326);
#326=ADVANCED_BREP_SHAPE_REPRESENTATION('',(#396),#15014);
#361=STYLED_ITEM('',(#15464),#396);
#396=MANIFOLD_SOLID_BREP('Body1',#7084);
#462=FACE_BOUND('',#1376,.T.);
#463=FACE_BOUND('',#1378,.T.);
#595=PLANE('',#7678);
#596=PLANE('',#7679);
#922=FACE_OUTER_BOUND('',#1373,.T.);
#923=FACE_OUTER_BOUND('',#1374,.T.);
#924=FACE_OUTER_BOUND('',#1375,.T.);
#925=FACE_OUTER_BOUND('',#1377,.T.);
#1373=EDGE_LOOP('',(#5172,#5173,#5174,#5175));
#1374=EDGE_LOOP('',(#5176,#5177,#5178,#5179));
#1375=EDGE_LOOP('',(#5180));
#1376=EDGE_LOOP('',(#5181));
#1377=EDGE_LOOP('',(#5182));
#1378=EDGE_LOOP('',(#5183));
#1879=LINE('',#10772,#2550);
#1880=LINE('',#10778,#2551);
#2550=VECTOR('',#8701,0.164999999999999);
#2551=VECTOR('',#8708,0.4);
#3157=CIRCLE('',#7673,0.164999999999999);
#3158=CIRCLE('',#7674,0.164999999999999);
#3159=CIRCLE('',#7676,0.4);
#3160=CIRCLE('',#7677,0.4);
#3434=VERTEX_POINT('',#10769);
#3435=VERTEX_POINT('',#10771);
#3436=VERTEX_POINT('',#10775);
#3437=VERTEX_POINT('',#10777);
#4087=EDGE_CURVE('',#3434,#3434,#3157,.T.);
#4088=EDGE_CURVE('',#3434,#3435,#1879,.T.);
#4089=EDGE_CURVE('',#3435,#3435,#3158,.T.);
#4090=EDGE_CURVE('',#3436,#3436,#3159,.T.);
#4091=EDGE_CURVE('',#3436,#3437,#1880,.T.);
#4092=EDGE_CURVE('',#3437,#3437,#3160,.T.);
#5172=ORIENTED_EDGE('',*,*,#4087,.F.);
#5173=ORIENTED_EDGE('',*,*,#4088,.T.);
#5174=ORIENTED_EDGE('',*,*,#4089,.T.);
#5175=ORIENTED_EDGE('',*,*,#4088,.F.);
#5176=ORIENTED_EDGE('',*,*,#4090,.F.);
#5177=ORIENTED_EDGE('',*,*,#4091,.T.);
#5178=ORIENTED_EDGE('',*,*,#4092,.T.);
#5179=ORIENTED_EDGE('',*,*,#4091,.F.);
#5180=ORIENTED_EDGE('',*,*,#4090,.T.);
#5181=ORIENTED_EDGE('',*,*,#4087,.T.);
#5182=ORIENTED_EDGE('',*,*,#4092,.F.);
#5183=ORIENTED_EDGE('',*,*,#4089,.F.);
#6606=CYLINDRICAL_SURFACE('',#7672,0.164999999999999);
#6607=CYLINDRICAL_SURFACE('',#7675,0.4);
#6764=ADVANCED_FACE('',(#922),#6606,.F.);
#6765=ADVANCED_FACE('',(#923),#6607,.T.);
#6766=ADVANCED_FACE('',(#924,#462),#595,.T.);
#6767=ADVANCED_FACE('',(#925,#463),#596,.F.);
#7084=CLOSED_SHELL('',(#6764,#6765,#6766,#6767));
#7671=AXIS2_PLACEMENT_3D('',#10767,#8695,#8696);
#7672=AXIS2_PLACEMENT_3D('',#10768,#8697,#8698);
#7673=AXIS2_PLACEMENT_3D('',#10770,#8699,#8700);
#7674=AXIS2_PLACEMENT_3D('',#10773,#8702,#8703);
#7675=AXIS2_PLACEMENT_3D('',#10774,#8704,#8705);
#7676=AXIS2_PLACEMENT_3D('',#10776,#8706,#8707);
#7677=AXIS2_PLACEMENT_3D('',#10779,#8709,#8710);
#7678=AXIS2_PLACEMENT_3D('',#10780,#8711,#8712);
#7679=AXIS2_PLACEMENT_3D('',#10781,#8713,#8714);
#8695=DIRECTION('axis',(0.,0.,1.));
#8696=DIRECTION('refdir',(1.,0.,0.));
#8697=DIRECTION('center_axis',(0.,0.,1.));
#8698=DIRECTION('ref_axis',(1.,0.,0.));
#8699=DIRECTION('center_axis',(0.,0.,-1.));
#8700=DIRECTION('ref_axis',(1.,0.,0.));
#8701=DIRECTION('',(0.,0.,-1.));
#8702=DIRECTION('center_axis',(0.,0.,-1.));
#8703=DIRECTION('ref_axis',(1.,0.,0.));
#8704=DIRECTION('center_axis',(0.,0.,1.));
#8705=DIRECTION('ref_axis',(1.,0.,0.));
#8706=DIRECTION('center_axis',(0.,0.,1.));
#8707=DIRECTION('ref_axis',(1.,0.,0.));
#8708=DIRECTION('',(0.,0.,-1.));
#8709=DIRECTION('center_axis',(0.,0.,1.));
#8710=DIRECTION('ref_axis',(1.,0.,0.));
#8711=DIRECTION('center_axis',(0.,0.,1.));
#8712=DIRECTION('ref_axis',(1.,0.,0.));
#8713=DIRECTION('center_axis',(0.,0.,1.));
#8714=DIRECTION('ref_axis',(1.,0.,0.));
#10767=CARTESIAN_POINT('',(0.,0.,0.));
#10768=CARTESIAN_POINT('Origin',(-8.8,0.,20.8));
#10769=CARTESIAN_POINT('',(-8.965,-2.02066721859312E-17,21.2));
#10770=CARTESIAN_POINT('Origin',(-8.8,0.,21.2));
#10771=CARTESIAN_POINT('',(-8.965,-2.02066721859312E-17,20.8));
#10772=CARTESIAN_POINT('',(-8.965,-2.02066721859312E-17,20.8));
#10773=CARTESIAN_POINT('Origin',(-8.8,0.,20.8));
#10774=CARTESIAN_POINT('Origin',(-8.8,0.,20.8));
#10775=CARTESIAN_POINT('',(-9.2,-4.89858719658942E-17,21.2));
#10776=CARTESIAN_POINT('Origin',(-8.8,0.,21.2));
#10777=CARTESIAN_POINT('',(-9.2,-4.89858719658942E-17,20.8));
#10778=CARTESIAN_POINT('',(-9.2,-4.89858719658942E-17,20.8));
#10779=CARTESIAN_POINT('Origin',(-8.8,0.,20.8));
#10780=CARTESIAN_POINT('Origin',(-8.8,0.,21.2));
#10781=CARTESIAN_POINT('Origin',(-8.8,0.,20.8));
#14974=UNCERTAINTY_MEASURE_WITH_UNIT(LENGTH_MEASURE(0.001),#15041,
'DISTANCE_ACCURACY_VALUE',
'Maximum model space distance between geometric entities at asserted c
onnectivities');
#15000=UNCERTAINTY_MEASURE_WITH_UNIT(LENGTH_MEASURE(0.001),#15041,
'DISTANCE_ACCURACY_VALUE',
'Maximum model space distance between geometric entities at asserted c
onnectivities');
#15014=(
GEOMETRIC_REPRESENTATION_CONTEXT(3)
GLOBAL_UNCERTAINTY_ASSIGNED_CONTEXT((#14974))
GLOBAL_UNIT_ASSIGNED_CONTEXT((#15041,#15043,#15044))
REPRESENTATION_CONTEXT('','3D')
);
#15040=(
GEOMETRIC_REPRESENTATION_CONTEXT(3)
GLOBAL_UNCERTAINTY_ASSIGNED_CONTEXT((#15000))
GLOBAL_UNIT_ASSIGNED_CONTEXT((#15041,#15043,#15044))
REPRESENTATION_CONTEXT('','3D')
);
#15041=(
LENGTH_UNIT()
NAMED_UNIT(*)
SI_UNIT(.CENTI.,.METRE.)
);
#15043=(
NAMED_UNIT(*)
PLANE_ANGLE_UNIT()
SI_UNIT($,.RADIAN.)
);
#15044=(
NAMED_UNIT(*)
SI_UNIT($,.STERADIAN.)
SOLID_ANGLE_UNIT()
);
#15058=SHAPE_DEFINITION_REPRESENTATION(#15097,#15195);
#15097=PRODUCT_DEFINITION_SHAPE('',$,#15235);
#15195=SHAPE_REPRESENTATION('',(#7671),#15014);
#15221=PRODUCT_DEFINITION_CONTEXT('part definition',#15340,'design');
#15235=PRODUCT_DEFINITION('M4 top nut','M4 top nut',#15274,#15221);
#15274=PRODUCT_DEFINITION_FORMATION('',$,#15355);
#15340=APPLICATION_CONTEXT(
'Core Data for Automotive Mechanical Design Process');
#15341=PRODUCT_CONTEXT('part definition',#15340,'mechanical');
#15355=PRODUCT('M4 top nut','M4 top nut','M4 top nut',(#15341));
#15458=COLOUR_RGB('Black',0.12,0.14,0.17);
#15459=FILL_AREA_STYLE_COLOUR('',#15458);
#15460=FILL_AREA_STYLE('',(#15459));
#15461=SURFACE_STYLE_FILL_AREA(#15460);
#15462=SURFACE_SIDE_STYLE('',(#15461));
#15463=SURFACE_STYLE_USAGE(.BOTH.,#15462);
#15464=PRESENTATION_STYLE_ASSIGNMENT((#15463));
ENDSEC;
END-ISO-10303-21;
